ISO-10303-21;
HEADER;
/* Generated by software containing ST-Developer
 * from STEP Tools, Inc. (www.steptools.com) 
 */

FILE_DESCRIPTION(
/* description */ ('PAT-001'),
/* implementation_level */ '2;1');

FILE_NAME(
/* name */ 'Take-up screw bracket (1).step',
/* time_stamp */ '2026-10-29T17:07:15-07:00',
/* author */ (''),
/* organization */ (''),
/* preprocessor_version */ 'ST-DEVELOPER v20.2',
/* originating_system */ 'Autodesk Translation Framework v15.17.0.0',
/* authorisation */ '');

FILE_SCHEMA (('AUTOMOTIVE_DESIGN { 1 0 10303 214 3 1 1 }'));
ENDSEC;

DATA;
#10=MECHANICAL_DESIGN_GEOMETRIC_PRESENTATION_REPRESENTATION('',(#394),#9622);
#336=SHAPE_REPRESENTATION_RELATIONSHIP('SRR','None',#9760,#361);
#361=ADVANCED_BREP_SHAPE_REPRESENTATION('',(#427),#9609);
#394=STYLED_ITEM('',(#9969),#427);
#427=MANIFOLD_SOLID_BREP('Body1',#5219);
#480=FACE_BOUND('',#1194,.T.);
#481=FACE_BOUND('',#1196,.T.);
#482=FACE_BOUND('',#1201,.T.);
#483=FACE_BOUND('',#1203,.T.);
#601=PLANE('',#5803);
#602=PLANE('',#5804);
#603=PLANE('',#5805);
#604=PLANE('',#5806);
#605=PLANE('',#5807);
#606=PLANE('',#5808);
#607=PLANE('',#5809);
#608=PLANE('',#5810);
#851=FACE_OUTER_BOUND('',#1190,.T.);
#852=FACE_OUTER_BOUND('',#1191,.T.);
#853=FACE_OUTER_BOUND('',#1192,.T.);
#854=FACE_OUTER_BOUND('',#1193,.T.);
#855=FACE_OUTER_BOUND('',#1195,.T.);
#856=FACE_OUTER_BOUND('',#1197,.T.);
#857=FACE_OUTER_BOUND('',#1198,.T.);
#858=FACE_OUTER_BOUND('',#1199,.T.);
#859=FACE_OUTER_BOUND('',#1200,.T.);
#860=FACE_OUTER_BOUND('',#1202,.T.);
#1190=EDGE_LOOP('',(#4083,#4084,#4085,#4086));
#1191=EDGE_LOOP('',(#4087,#4088,#4089,#4090));
#1192=EDGE_LOOP('',(#4091,#4092,#4093,#4094));
#1193=EDGE_LOOP('',(#4095,#4096,#4097,#4098));
#1194=EDGE_LOOP('',(#4099));
#1195=EDGE_LOOP('',(#4100,#4101,#4102,#4103));
#1196=EDGE_LOOP('',(#4104));
#1197=EDGE_LOOP('',(#4105,#4106,#4107,#4108,#4109,#4110));
#1198=EDGE_LOOP('',(#4111,#4112,#4113,#4114,#4115,#4116));
#1199=EDGE_LOOP('',(#4117,#4118,#4119,#4120));
#1200=EDGE_LOOP('',(#4121,#4122,#4123,#4124));
#1201=EDGE_LOOP('',(#4125));
#1202=EDGE_LOOP('',(#4126,#4127,#4128,#4129));
#1203=EDGE_LOOP('',(#4130));
#1533=LINE('',#8689,#1938);
#1534=LINE('',#8695,#1939);
#1535=LINE('',#8700,#1940);
#1536=LINE('',#8702,#1941);
#1537=LINE('',#8704,#1942);
#1538=LINE('',#8705,#1943);
#1539=LINE('',#8709,#1944);
#1540=LINE('',#8710,#1945);
#1541=LINE('',#8711,#1946);
#1542=LINE('',#8714,#1947);
#1543=LINE('',#8716,#1948);
#1544=LINE('',#8717,#1949);
#1545=LINE('',#8720,#1950);
#1546=LINE('',#8722,#1951);
#1547=LINE('',#8723,#1952);
#1548=LINE('',#8726,#1953);
#1549=LINE('',#8728,#1954);
#1550=LINE('',#8729,#1955);
#1551=LINE('',#8731,#1956);
#1552=LINE('',#8733,#1957);
#1938=VECTOR('',#6822,0.275);
#1939=VECTOR('',#6829,0.34);
#1940=VECTOR('',#6834,1.);
#1941=VECTOR('',#6835,1.);
#1942=VECTOR('',#6836,1.);
#1943=VECTOR('',#6837,1.);
#1944=VECTOR('',#6840,1.);
#1945=VECTOR('',#6841,1.);
#1946=VECTOR('',#6842,1.);
#1947=VECTOR('',#6845,1.);
#1948=VECTOR('',#6846,1.);
#1949=VECTOR('',#6847,1.);
#1950=VECTOR('',#6850,1.);
#1951=VECTOR('',#6851,1.);
#1952=VECTOR('',#6852,1.);
#1953=VECTOR('',#6855,1.);
#1954=VECTOR('',#6856,1.);
#1955=VECTOR('',#6857,1.);
#1956=VECTOR('',#6860,1.);
#1957=VECTOR('',#6863,1.);
#2338=CIRCLE('',#5798,0.275);
#2339=CIRCLE('',#5799,0.275);
#2340=CIRCLE('',#5801,0.34);
#2341=CIRCLE('',#5802,0.34);
#2618=VERTEX_POINT('',#8686);
#2619=VERTEX_POINT('',#8688);
#2620=VERTEX_POINT('',#8692);
#2621=VERTEX_POINT('',#8694);
#2622=VERTEX_POINT('',#8698);
#2623=VERTEX_POINT('',#8699);
#2624=VERTEX_POINT('',#8701);
#2625=VERTEX_POINT('',#8703);
#2626=VERTEX_POINT('',#8707);
#2627=VERTEX_POINT('',#8708);
#2628=VERTEX_POINT('',#8713);
#2629=VERTEX_POINT('',#8715);
#2630=VERTEX_POINT('',#8719);
#2631=VERTEX_POINT('',#8721);
#2632=VERTEX_POINT('',#8725);
#2633=VERTEX_POINT('',#8727);
#3145=EDGE_CURVE('',#2618,#2618,#2338,.T.);
#3146=EDGE_CURVE('',#2618,#2619,#1533,.T.);
#3147=EDGE_CURVE('',#2619,#2619,#2339,.T.);
#3148=EDGE_CURVE('',#2620,#2620,#2340,.T.);
#3149=EDGE_CURVE('',#2620,#2621,#1534,.T.);
#3150=EDGE_CURVE('',#2621,#2621,#2341,.T.);
#3151=EDGE_CURVE('',#2622,#2623,#1535,.T.);
#3152=EDGE_CURVE('',#2623,#2624,#1536,.T.);
#3153=EDGE_CURVE('',#2625,#2624,#1537,.T.);
#3154=EDGE_CURVE('',#2622,#2625,#1538,.T.);
#3155=EDGE_CURVE('',#2626,#2627,#1539,.T.);
#3156=EDGE_CURVE('',#2626,#2625,#1540,.T.);
#3157=EDGE_CURVE('',#2624,#2627,#1541,.T.);
#3158=EDGE_CURVE('',#2627,#2628,#1542,.T.);
#3159=EDGE_CURVE('',#2628,#2629,#1543,.T.);
#3160=EDGE_CURVE('',#2629,#2626,#1544,.T.);
#3161=EDGE_CURVE('',#2630,#2623,#1545,.T.);
#3162=EDGE_CURVE('',#2630,#2631,#1546,.T.);
#3163=EDGE_CURVE('',#2631,#2628,#1547,.T.);
#3164=EDGE_CURVE('',#2632,#2629,#1548,.T.);
#3165=EDGE_CURVE('',#2632,#2633,#1549,.T.);
#3166=EDGE_CURVE('',#2633,#2622,#1550,.T.);
#3167=EDGE_CURVE('',#2631,#2632,#1551,.T.);
#3168=EDGE_CURVE('',#2633,#2630,#1552,.T.);
#4083=ORIENTED_EDGE('',*,*,#3145,.F.);
#4084=ORIENTED_EDGE('',*,*,#3146,.T.);
#4085=ORIENTED_EDGE('',*,*,#3147,.F.);
#4086=ORIENTED_EDGE('',*,*,#3146,.F.);
#4087=ORIENTED_EDGE('',*,*,#3148,.F.);
#4088=ORIENTED_EDGE('',*,*,#3149,.T.);
#4089=ORIENTED_EDGE('',*,*,#3150,.F.);
#4090=ORIENTED_EDGE('',*,*,#3149,.F.);
#4091=ORIENTED_EDGE('',*,*,#3151,.T.);
#4092=ORIENTED_EDGE('',*,*,#3152,.T.);
#4093=ORIENTED_EDGE('',*,*,#3153,.F.);
#4094=ORIENTED_EDGE('',*,*,#3154,.F.);
#4095=ORIENTED_EDGE('',*,*,#3155,.F.);
#4096=ORIENTED_EDGE('',*,*,#3156,.T.);
#4097=ORIENTED_EDGE('',*,*,#3153,.T.);
#4098=ORIENTED_EDGE('',*,*,#3157,.T.);
#4099=ORIENTED_EDGE('',*,*,#3150,.T.);
#4100=ORIENTED_EDGE('',*,*,#3155,.T.);
#4101=ORIENTED_EDGE('',*,*,#3158,.T.);
#4102=ORIENTED_EDGE('',*,*,#3159,.T.);
#4103=ORIENTED_EDGE('',*,*,#3160,.T.);
#4104=ORIENTED_EDGE('',*,*,#3147,.T.);
#4105=ORIENTED_EDGE('',*,*,#3161,.F.);
#4106=ORIENTED_EDGE('',*,*,#3162,.T.);
#4107=ORIENTED_EDGE('',*,*,#3163,.T.);
#4108=ORIENTED_EDGE('',*,*,#3158,.F.);
#4109=ORIENTED_EDGE('',*,*,#3157,.F.);
#4110=ORIENTED_EDGE('',*,*,#3152,.F.);
#4111=ORIENTED_EDGE('',*,*,#3160,.F.);
#4112=ORIENTED_EDGE('',*,*,#3164,.F.);
#4113=ORIENTED_EDGE('',*,*,#3165,.T.);
#4114=ORIENTED_EDGE('',*,*,#3166,.T.);
#4115=ORIENTED_EDGE('',*,*,#3154,.T.);
#4116=ORIENTED_EDGE('',*,*,#3156,.F.);
#4117=ORIENTED_EDGE('',*,*,#3167,.T.);
#4118=ORIENTED_EDGE('',*,*,#3164,.T.);
#4119=ORIENTED_EDGE('',*,*,#3159,.F.);
#4120=ORIENTED_EDGE('',*,*,#3163,.F.);
#4121=ORIENTED_EDGE('',*,*,#3166,.F.);
#4122=ORIENTED_EDGE('',*,*,#3168,.T.);
#4123=ORIENTED_EDGE('',*,*,#3161,.T.);
#4124=ORIENTED_EDGE('',*,*,#3151,.F.);
#4125=ORIENTED_EDGE('',*,*,#3148,.T.);
#4126=ORIENTED_EDGE('',*,*,#3168,.F.);
#4127=ORIENTED_EDGE('',*,*,#3165,.F.);
#4128=ORIENTED_EDGE('',*,*,#3167,.F.);
#4129=ORIENTED_EDGE('',*,*,#3162,.F.);
#4130=ORIENTED_EDGE('',*,*,#3145,.T.);
#4868=CYLINDRICAL_SURFACE('',#5797,0.275);
#4869=CYLINDRICAL_SURFACE('',#5800,0.34);
#5038=ADVANCED_FACE('',(#851),#4868,.F.);
#5039=ADVANCED_FACE('',(#852),#4869,.F.);
#5040=ADVANCED_FACE('',(#853),#601,.T.);
#5041=ADVANCED_FACE('',(#854,#480),#602,.T.);
#5042=ADVANCED_FACE('',(#855,#481),#603,.T.);
#5043=ADVANCED_FACE('',(#856),#604,.T.);
#5044=ADVANCED_FACE('',(#857),#605,.T.);
#5045=ADVANCED_FACE('',(#858),#606,.T.);
#5046=ADVANCED_FACE('',(#859,#482),#607,.T.);
#5047=ADVANCED_FACE('',(#860,#483),#608,.F.);
#5219=CLOSED_SHELL('',(#5038,#5039,#5040,#5041,#5042,#5043,#5044,#5045,
#5046,#5047));
#5796=AXIS2_PLACEMENT_3D('',#8684,#6816,#6817);
#5797=AXIS2_PLACEMENT_3D('',#8685,#6818,#6819);
#5798=AXIS2_PLACEMENT_3D('',#8687,#6820,#6821);
#5799=AXIS2_PLACEMENT_3D('',#8690,#6823,#6824);
#5800=AXIS2_PLACEMENT_3D('',#8691,#6825,#6826);
#5801=AXIS2_PLACEMENT_3D('',#8693,#6827,#6828);
#5802=AXIS2_PLACEMENT_3D('',#8696,#6830,#6831);
#5803=AXIS2_PLACEMENT_3D('',#8697,#6832,#6833);
#5804=AXIS2_PLACEMENT_3D('',#8706,#6838,#6839);
#5805=AXIS2_PLACEMENT_3D('',#8712,#6843,#6844);
#5806=AXIS2_PLACEMENT_3D('',#8718,#6848,#6849);
#5807=AXIS2_PLACEMENT_3D('',#8724,#6853,#6854);
#5808=AXIS2_PLACEMENT_3D('',#8730,#6858,#6859);
#5809=AXIS2_PLACEMENT_3D('',#8732,#6861,#6862);
#5810=AXIS2_PLACEMENT_3D('',#8734,#6864,#6865);
#6816=DIRECTION('axis',(0.,0.,1.));
#6817=DIRECTION('refdir',(1.,0.,0.));
#6818=DIRECTION('center_axis',(0.,0.,1.));
#6819=DIRECTION('ref_axis',(1.,0.,0.));
#6820=DIRECTION('center_axis',(0.,0.,1.));
#6821=DIRECTION('ref_axis',(1.,0.,0.));
#6822=DIRECTION('',(0.,0.,1.));
#6823=DIRECTION('center_axis',(0.,0.,-1.));
#6824=DIRECTION('ref_axis',(1.,0.,0.));
#6825=DIRECTION('center_axis',(1.,0.,0.));
#6826=DIRECTION('ref_axis',(0.,0.,-1.));
#6827=DIRECTION('center_axis',(1.,0.,0.));
#6828=DIRECTION('ref_axis',(0.,0.,-1.));
#6829=DIRECTION('',(1.,0.,0.));
#6830=DIRECTION('center_axis',(-1.,0.,0.));
#6831=DIRECTION('ref_axis',(0.,0.,-1.));
#6832=DIRECTION('center_axis',(0.,0.,1.));
#6833=DIRECTION('ref_axis',(0.,-1.,0.));
#6834=DIRECTION('',(0.,-1.,0.));
#6835=DIRECTION('',(1.,0.,0.));
#6836=DIRECTION('',(0.,-1.,0.));
#6837=DIRECTION('',(1.,0.,0.));
#6838=DIRECTION('center_axis',(1.,0.,0.));
#6839=DIRECTION('ref_axis',(0.,0.,-1.));
#6840=DIRECTION('',(0.,-1.,0.));
#6841=DIRECTION('',(0.,0.,1.));
#6842=DIRECTION('',(0.,0.,-1.));
#6843=DIRECTION('center_axis',(0.,0.,1.));
#6844=DIRECTION('ref_axis',(1.,0.,0.));
#6845=DIRECTION('',(1.,0.,0.));
#6846=DIRECTION('',(0.,1.,0.));
#6847=DIRECTION('',(-1.,0.,0.));
#6848=DIRECTION('center_axis',(0.,-1.,0.));
#6849=DIRECTION('ref_axis',(1.,0.,0.));
#6850=DIRECTION('',(0.,0.,1.));
#6851=DIRECTION('',(1.,0.,0.));
#6852=DIRECTION('',(0.,0.,1.));
#6853=DIRECTION('center_axis',(0.,1.,0.));
#6854=DIRECTION('ref_axis',(-1.,0.,0.));
#6855=DIRECTION('',(0.,0.,1.));
#6856=DIRECTION('',(-1.,0.,0.));
#6857=DIRECTION('',(0.,0.,1.));
#6858=DIRECTION('center_axis',(1.,0.,0.));
#6859=DIRECTION('ref_axis',(0.,1.,0.));
#6860=DIRECTION('',(0.,1.,0.));
#6861=DIRECTION('center_axis',(-1.,0.,0.));
#6862=DIRECTION('ref_axis',(0.,-1.,0.));
#6863=DIRECTION('',(0.,-1.,0.));
#6864=DIRECTION('center_axis',(0.,0.,1.));
#6865=DIRECTION('ref_axis',(1.,0.,0.));
#8684=CARTESIAN_POINT('',(0.,0.,0.));
#8685=CARTESIAN_POINT('Origin',(-3.5,32.,1.9));
#8686=CARTESIAN_POINT('',(-3.775,32.,2.));
#8687=CARTESIAN_POINT('Origin',(-3.5,32.,2.));
#8688=CARTESIAN_POINT('',(-3.775,32.,2.8));
#8689=CARTESIAN_POINT('',(-3.775,32.,1.9));
#8690=CARTESIAN_POINT('Origin',(-3.5,32.,2.8));
#8691=CARTESIAN_POINT('Origin',(-5.1,32.,4.5));
#8692=CARTESIAN_POINT('',(-5.,32.,4.84));
#8693=CARTESIAN_POINT('Origin',(-5.,32.,4.5));
#8694=CARTESIAN_POINT('',(-4.2,32.,4.84));
#8695=CARTESIAN_POINT('',(-5.1,32.,4.84));
#8696=CARTESIAN_POINT('Origin',(-4.2,32.,4.5));
#8697=CARTESIAN_POINT('Origin',(-5.,33.2,5.5));
#8698=CARTESIAN_POINT('',(-5.,33.2,5.5));
#8699=CARTESIAN_POINT('',(-5.,30.8,5.5));
#8700=CARTESIAN_POINT('',(-5.,33.2,5.5));
#8701=CARTESIAN_POINT('',(-4.2,30.8,5.5));
#8702=CARTESIAN_POINT('',(-5.,30.8,5.5));
#8703=CARTESIAN_POINT('',(-4.2,33.2,5.5));
#8704=CARTESIAN_POINT('',(-4.2,33.2,5.5));
#8705=CARTESIAN_POINT('',(-5.,33.2,5.5));
#8706=CARTESIAN_POINT('Origin',(-4.2,32.,4.1));
#8707=CARTESIAN_POINT('',(-4.2,33.2,2.8));
#8708=CARTESIAN_POINT('',(-4.2,30.8,2.8));
#8709=CARTESIAN_POINT('',(-4.2,32.,2.8));
#8710=CARTESIAN_POINT('',(-4.2,33.2,2.7));
#8711=CARTESIAN_POINT('',(-4.2,30.8,5.5));
#8712=CARTESIAN_POINT('Origin',(-4.,32.,2.8));
#8713=CARTESIAN_POINT('',(-3.,30.8,2.8));
#8714=CARTESIAN_POINT('',(-5.,30.8,2.8));
#8715=CARTESIAN_POINT('',(-3.,33.2,2.8));
#8716=CARTESIAN_POINT('',(-3.,30.8,2.8));
#8717=CARTESIAN_POINT('',(-3.,33.2,2.8));
#8718=CARTESIAN_POINT('Origin',(-5.,30.8,2.));
#8719=CARTESIAN_POINT('',(-5.,30.8,2.));
#8720=CARTESIAN_POINT('',(-5.,30.8,2.));
#8721=CARTESIAN_POINT('',(-3.,30.8,2.));
#8722=CARTESIAN_POINT('',(-5.,30.8,2.));
#8723=CARTESIAN_POINT('',(-3.,30.8,2.));
#8724=CARTESIAN_POINT('Origin',(-3.,33.2,2.));
#8725=CARTESIAN_POINT('',(-3.,33.2,2.));
#8726=CARTESIAN_POINT('',(-3.,33.2,2.));
#8727=CARTESIAN_POINT('',(-5.,33.2,2.));
#8728=CARTESIAN_POINT('',(-3.,33.2,2.));
#8729=CARTESIAN_POINT('',(-5.,33.2,2.));
#8730=CARTESIAN_POINT('Origin',(-3.,30.8,2.));
#8731=CARTESIAN_POINT('',(-3.,30.8,2.));
#8732=CARTESIAN_POINT('Origin',(-5.,33.2,2.));
#8733=CARTESIAN_POINT('',(-5.,33.2,2.));
#8734=CARTESIAN_POINT('Origin',(-4.,32.,2.));
#9579=UNCERTAINTY_MEASURE_WITH_UNIT(LENGTH_MEASURE(0.001),#9623,
'DISTANCE_ACCURACY_VALUE',
'Maximum model space distance between geometric entities at asserted c
onnectivities');
#9592=UNCERTAINTY_MEASURE_WITH_UNIT(LENGTH_MEASURE(0.001),#9623,
'DISTANCE_ACCURACY_VALUE',
'Maximum model space distance between geometric entities at asserted c
onnectivities');
#9609=(
GEOMETRIC_REPRESENTATION_CONTEXT(3)
GLOBAL_UNCERTAINTY_ASSIGNED_CONTEXT((#9579))
GLOBAL_UNIT_ASSIGNED_CONTEXT((#9623,#9625,#9626))
REPRESENTATION_CONTEXT('','3D')
);
#9622=(
GEOMETRIC_REPRESENTATION_CONTEXT(3)
GLOBAL_UNCERTAINTY_ASSIGNED_CONTEXT((#9592))
GLOBAL_UNIT_ASSIGNED_CONTEXT((#9623,#9625,#9626))
REPRESENTATION_CONTEXT('','3D')
);
#9623=(
LENGTH_UNIT()
NAMED_UNIT(*)
SI_UNIT(.CENTI.,.METRE.)
);
#9625=(
NAMED_UNIT(*)
PLANE_ANGLE_UNIT()
SI_UNIT($,.RADIAN.)
);
#9626=(
NAMED_UNIT(*)
SI_UNIT($,.STERADIAN.)
SOLID_ANGLE_UNIT()
);
#9643=SHAPE_DEFINITION_REPRESENTATION(#9677,#9760);
#9677=PRODUCT_DEFINITION_SHAPE('',$,#9790);
#9760=SHAPE_REPRESENTATION('',(#5796),#9609);
#9773=PRODUCT_DEFINITION_CONTEXT('part definition',#9862,'design');
#9790=PRODUCT_DEFINITION('Take-up screw bracket (1)',
'Take-up screw bracket (1)',#9819,#9773);
#9819=PRODUCT_DEFINITION_FORMATION('',$,#9880);
#9862=APPLICATION_CONTEXT(
'Core Data for Automotive Mechanical Design Process');
#9863=PRODUCT_CONTEXT('part definition',#9862,'mechanical');
#9880=PRODUCT('Take-up screw bracket (1)','Take-up screw bracket (1)',
'Take-up screw bracket (1)',(#9863));
#9963=COLOUR_RGB('Black',0.12,0.14,0.17);
#9964=FILL_AREA_STYLE_COLOUR('',#9963);
#9965=FILL_AREA_STYLE('',(#9964));
#9966=SURFACE_STYLE_FILL_AREA(#9965);
#9967=SURFACE_SIDE_STYLE('',(#9966));
#9968=SURFACE_STYLE_USAGE(.BOTH.,#9967);
#9969=PRESENTATION_STYLE_ASSIGNMENT((#9968));
ENDSEC;
END-ISO-10303-21;
